ISO-10303-21;
HEADER;
/* Generated by software containing ST-Developer
 * from STEP Tools, Inc. (www.steptools.com) 
 */

FILE_DESCRIPTION(
/* description */ ('Rigid flange shaft coupling assembly'),
/* implementation_level */ '2;1');

FILE_NAME(
/* name */ 'Shaft stub (1).step',
/* time_stamp */ '2026-10-27T10:47:16-07:00',
/* author */ (''),
/* organization */ (''),
/* preprocessor_version */ 'ST-DEVELOPER v20.2',
/* originating_system */ 'Autodesk Translation Framework v15.17.0.0',
/* authorisation */ '');

FILE_SCHEMA (('AUTOMOTIVE_DESIGN { 1 0 10303 214 3 1 1 }'));
ENDSEC;

DATA;
#10=MECHANICAL_DESIGN_GEOMETRIC_PRESENTATION_REPRESENTATION('',(#415),#9141);
#358=SHAPE_REPRESENTATION_RELATIONSHIP('SRR','None',#9294,#386);
#386=ADVANCED_BREP_SHAPE_REPRESENTATION('',(#443),#9129);
#415=STYLED_ITEM('',(#9500),#443);
#443=MANIFOLD_SOLID_BREP('Body1',#4770);
#535=FACE_BOUND('',#1257,.T.);
#536=FACE_BOUND('',#1259,.T.);
#664=PLANE('',#5376);
#665=PLANE('',#5377);
#666=PLANE('',#5378);
#667=PLANE('',#5380);
#668=PLANE('',#5381);
#669=PLANE('',#5382);
#670=PLANE('',#5387);
#671=PLANE('',#5388);
#895=FACE_OUTER_BOUND('',#1249,.T.);
#896=FACE_OUTER_BOUND('',#1250,.T.);
#897=FACE_OUTER_BOUND('',#1251,.T.);
#898=FACE_OUTER_BOUND('',#1252,.T.);
#899=FACE_OUTER_BOUND('',#1253,.T.);
#900=FACE_OUTER_BOUND('',#1254,.T.);
#901=FACE_OUTER_BOUND('',#1255,.T.);
#902=FACE_OUTER_BOUND('',#1256,.T.);
#903=FACE_OUTER_BOUND('',#1258,.T.);
#904=FACE_OUTER_BOUND('',#1260,.T.);
#1249=EDGE_LOOP('',(#3901,#3902,#3903,#3904));
#1250=EDGE_LOOP('',(#3905));
#1251=EDGE_LOOP('',(#3906,#3907,#3908,#3909));
#1252=EDGE_LOOP('',(#3910,#3911,#3912,#3913));
#1253=EDGE_LOOP('',(#3914,#3915,#3916,#3917));
#1254=EDGE_LOOP('',(#3918,#3919,#3920,#3921));
#1255=EDGE_LOOP('',(#3922,#3923,#3924,#3925));
#1256=EDGE_LOOP('',(#3926,#3927,#3928,#3929));
#1257=EDGE_LOOP('',(#3930,#3931,#3932,#3933));
#1258=EDGE_LOOP('',(#3934));
#1259=EDGE_LOOP('',(#3935));
#1260=EDGE_LOOP('',(#3936));
#1600=LINE('',#8278,#1945);
#1601=LINE('',#8284,#1946);
#1602=LINE('',#8286,#1947);
#1603=LINE('',#8288,#1948);
#1604=LINE('',#8289,#1949);
#1605=LINE('',#8294,#1950);
#1606=LINE('',#8295,#1951);
#1607=LINE('',#8298,#1952);
#1608=LINE('',#8300,#1953);
#1609=LINE('',#8301,#1954);
#1610=LINE('',#8303,#1955);
#1611=LINE('',#8310,#1956);
#1945=VECTOR('',#6401,0.21);
#1946=VECTOR('',#6408,1.);
#1947=VECTOR('',#6409,1.);
#1948=VECTOR('',#6410,1.);
#1949=VECTOR('',#6411,1.);
#1950=VECTOR('',#6416,1.);
#1951=VECTOR('',#6417,1.);
#1952=VECTOR('',#6420,1.);
#1953=VECTOR('',#6421,1.);
#1954=VECTOR('',#6422,1.);
#1955=VECTOR('',#6425,1.);
#1956=VECTOR('',#6434,1.);
#2201=CIRCLE('',#5374,0.21);
#2202=CIRCLE('',#5375,0.21);
#2203=CIRCLE('',#5379,1.);
#2204=CIRCLE('',#5383,1.);
#2205=CIRCLE('',#5385,1.);
#2206=CIRCLE('',#5386,1.);
#2502=VERTEX_POINT('',#8275);
#2503=VERTEX_POINT('',#8277);
#2504=VERTEX_POINT('',#8282);
#2505=VERTEX_POINT('',#8283);
#2506=VERTEX_POINT('',#8285);
#2507=VERTEX_POINT('',#8287);
#2508=VERTEX_POINT('',#8291);
#2509=VERTEX_POINT('',#8293);
#2510=VERTEX_POINT('',#8297);
#2511=VERTEX_POINT('',#8299);
#2512=VERTEX_POINT('',#8307);
#2513=VERTEX_POINT('',#8309);
#2994=EDGE_CURVE('',#2502,#2502,#2201,.T.);
#2995=EDGE_CURVE('',#2502,#2503,#1600,.T.);
#2996=EDGE_CURVE('',#2503,#2503,#2202,.T.);
#2997=EDGE_CURVE('',#2504,#2505,#1601,.T.);
#2998=EDGE_CURVE('',#2504,#2506,#1602,.T.);
#2999=EDGE_CURVE('',#2507,#2506,#1603,.T.);
#3000=EDGE_CURVE('',#2507,#2505,#1604,.T.);
#3001=EDGE_CURVE('',#2505,#2508,#2203,.T.);
#3002=EDGE_CURVE('',#2509,#2507,#1605,.T.);
#3003=EDGE_CURVE('',#2508,#2509,#1606,.T.);
#3004=EDGE_CURVE('',#2508,#2510,#1607,.T.);
#3005=EDGE_CURVE('',#2509,#2511,#1608,.T.);
#3006=EDGE_CURVE('',#2511,#2510,#1609,.T.);
#3007=EDGE_CURVE('',#2506,#2511,#1610,.T.);
#3008=EDGE_CURVE('',#2510,#2504,#2204,.T.);
#3009=EDGE_CURVE('',#2512,#2512,#2205,.T.);
#3010=EDGE_CURVE('',#2512,#2513,#1611,.T.);
#3011=EDGE_CURVE('',#2513,#2513,#2206,.T.);
#3901=ORIENTED_EDGE('',*,*,#2994,.F.);
#3902=ORIENTED_EDGE('',*,*,#2995,.T.);
#3903=ORIENTED_EDGE('',*,*,#2996,.F.);
#3904=ORIENTED_EDGE('',*,*,#2995,.F.);
#3905=ORIENTED_EDGE('',*,*,#2994,.T.);
#3906=ORIENTED_EDGE('',*,*,#2997,.F.);
#3907=ORIENTED_EDGE('',*,*,#2998,.T.);
#3908=ORIENTED_EDGE('',*,*,#2999,.F.);
#3909=ORIENTED_EDGE('',*,*,#3000,.T.);
#3910=ORIENTED_EDGE('',*,*,#3001,.F.);
#3911=ORIENTED_EDGE('',*,*,#3000,.F.);
#3912=ORIENTED_EDGE('',*,*,#3002,.F.);
#3913=ORIENTED_EDGE('',*,*,#3003,.F.);
#3914=ORIENTED_EDGE('',*,*,#3004,.F.);
#3915=ORIENTED_EDGE('',*,*,#3003,.T.);
#3916=ORIENTED_EDGE('',*,*,#3005,.T.);
#3917=ORIENTED_EDGE('',*,*,#3006,.T.);
#3918=ORIENTED_EDGE('',*,*,#3002,.T.);
#3919=ORIENTED_EDGE('',*,*,#2999,.T.);
#3920=ORIENTED_EDGE('',*,*,#3007,.T.);
#3921=ORIENTED_EDGE('',*,*,#3005,.F.);
#3922=ORIENTED_EDGE('',*,*,#3008,.F.);
#3923=ORIENTED_EDGE('',*,*,#3006,.F.);
#3924=ORIENTED_EDGE('',*,*,#3007,.F.);
#3925=ORIENTED_EDGE('',*,*,#2998,.F.);
#3926=ORIENTED_EDGE('',*,*,#3009,.F.);
#3927=ORIENTED_EDGE('',*,*,#3010,.T.);
#3928=ORIENTED_EDGE('',*,*,#3011,.T.);
#3929=ORIENTED_EDGE('',*,*,#3010,.F.);
#3930=ORIENTED_EDGE('',*,*,#3004,.T.);
#3931=ORIENTED_EDGE('',*,*,#3008,.T.);
#3932=ORIENTED_EDGE('',*,*,#2997,.T.);
#3933=ORIENTED_EDGE('',*,*,#3001,.T.);
#3934=ORIENTED_EDGE('',*,*,#3009,.T.);
#3935=ORIENTED_EDGE('',*,*,#2996,.T.);
#3936=ORIENTED_EDGE('',*,*,#3011,.F.);
#4451=CYLINDRICAL_SURFACE('',#5373,0.21);
#4452=CYLINDRICAL_SURFACE('',#5384,1.);
#4631=ADVANCED_FACE('',(#895),#4451,.F.);
#4632=ADVANCED_FACE('',(#896),#664,.T.);
#4633=ADVANCED_FACE('',(#897),#665,.F.);
#4634=ADVANCED_FACE('',(#898),#666,.T.);
#4635=ADVANCED_FACE('',(#899),#667,.F.);
#4636=ADVANCED_FACE('',(#900),#668,.F.);
#4637=ADVANCED_FACE('',(#901),#669,.F.);
#4638=ADVANCED_FACE('',(#902,#535),#4452,.T.);
#4639=ADVANCED_FACE('',(#903,#536),#670,.T.);
#4640=ADVANCED_FACE('',(#904),#671,.F.);
#4770=CLOSED_SHELL('',(#4631,#4632,#4633,#4634,#4635,#4636,#4637,#4638,
#4639,#4640));
#5372=AXIS2_PLACEMENT_3D('',#8273,#6395,#6396);
#5373=AXIS2_PLACEMENT_3D('',#8274,#6397,#6398);
#5374=AXIS2_PLACEMENT_3D('',#8276,#6399,#6400);
#5375=AXIS2_PLACEMENT_3D('',#8279,#6402,#6403);
#5376=AXIS2_PLACEMENT_3D('',#8280,#6404,#6405);
#5377=AXIS2_PLACEMENT_3D('',#8281,#6406,#6407);
#5378=AXIS2_PLACEMENT_3D('',#8290,#6412,#6413);
#5379=AXIS2_PLACEMENT_3D('',#8292,#6414,#6415);
#5380=AXIS2_PLACEMENT_3D('',#8296,#6418,#6419);
#5381=AXIS2_PLACEMENT_3D('',#8302,#6423,#6424);
#5382=AXIS2_PLACEMENT_3D('',#8304,#6426,#6427);
#5383=AXIS2_PLACEMENT_3D('',#8305,#6428,#6429);
#5384=AXIS2_PLACEMENT_3D('',#8306,#6430,#6431);
#5385=AXIS2_PLACEMENT_3D('',#8308,#6432,#6433);
#5386=AXIS2_PLACEMENT_3D('',#8311,#6435,#6436);
#5387=AXIS2_PLACEMENT_3D('',#8312,#6437,#6438);
#5388=AXIS2_PLACEMENT_3D('',#8313,#6439,#6440);
#6395=DIRECTION('axis',(0.,0.,1.));
#6396=DIRECTION('refdir',(1.,0.,0.));
#6397=DIRECTION('center_axis',(0.,1.,0.));
#6398=DIRECTION('ref_axis',(1.,0.,0.));
#6399=DIRECTION('center_axis',(0.,1.,0.));
#6400=DIRECTION('ref_axis',(1.,0.,0.));
#6401=DIRECTION('',(0.,1.,0.));
#6402=DIRECTION('center_axis',(0.,-1.,0.));
#6403=DIRECTION('ref_axis',(1.,0.,0.));
#6404=DIRECTION('center_axis',(0.,1.,0.));
#6405=DIRECTION('ref_axis',(1.,0.,0.));
#6406=DIRECTION('center_axis',(-1.,0.,0.));
#6407=DIRECTION('ref_axis',(0.,0.,1.));
#6408=DIRECTION('',(0.,-1.,0.));
#6409=DIRECTION('',(0.,0.,1.));
#6410=DIRECTION('',(0.,1.,0.));
#6411=DIRECTION('',(0.,0.,-1.));
#6412=DIRECTION('center_axis',(0.,1.,0.));
#6413=DIRECTION('ref_axis',(1.,0.,0.));
#6414=DIRECTION('center_axis',(0.,-1.,0.));
#6415=DIRECTION('ref_axis',(1.,0.,0.));
#6416=DIRECTION('',(-1.,0.,0.));
#6417=DIRECTION('',(0.,0.,1.));
#6418=DIRECTION('center_axis',(1.,0.,0.));
#6419=DIRECTION('ref_axis',(0.,0.,-1.));
#6420=DIRECTION('',(0.,1.,0.));
#6421=DIRECTION('',(0.,1.,0.));
#6422=DIRECTION('',(0.,0.,-1.));
#6423=DIRECTION('center_axis',(0.,0.,1.));
#6424=DIRECTION('ref_axis',(1.,0.,0.));
#6425=DIRECTION('',(1.,0.,0.));
#6426=DIRECTION('center_axis',(0.,1.,0.));
#6427=DIRECTION('ref_axis',(0.,0.,1.));
#6428=DIRECTION('center_axis',(0.,1.,0.));
#6429=DIRECTION('ref_axis',(1.,0.,0.));
#6430=DIRECTION('center_axis',(0.,1.,0.));
#6431=DIRECTION('ref_axis',(1.,0.,0.));
#6432=DIRECTION('center_axis',(0.,1.,0.));
#6433=DIRECTION('ref_axis',(1.,0.,0.));
#6434=DIRECTION('',(0.,-1.,0.));
#6435=DIRECTION('center_axis',(0.,1.,0.));
#6436=DIRECTION('ref_axis',(1.,0.,0.));
#6437=DIRECTION('center_axis',(0.,1.,0.));
#6438=DIRECTION('ref_axis',(1.,0.,0.));
#6439=DIRECTION('center_axis',(0.,1.,0.));
#6440=DIRECTION('ref_axis',(1.,0.,0.));
#8273=CARTESIAN_POINT('',(0.,0.,0.));
#8274=CARTESIAN_POINT('Origin',(0.,22.5,6.53));
#8275=CARTESIAN_POINT('',(-0.21,22.5,6.53));
#8276=CARTESIAN_POINT('Origin',(0.,22.5,6.53));
#8277=CARTESIAN_POINT('',(-0.21,24.5,6.53));
#8278=CARTESIAN_POINT('',(-0.21,22.5,6.53));
#8279=CARTESIAN_POINT('Origin',(0.,24.5,6.53));
#8280=CARTESIAN_POINT('Origin',(0.,22.5,6.53));
#8281=CARTESIAN_POINT('Origin',(-0.3,10.8,5.43));
#8282=CARTESIAN_POINT('',(-0.3,12.8,5.57606079858305));
#8283=CARTESIAN_POINT('',(-0.3,10.8,5.57606079858305));
#8284=CARTESIAN_POINT('',(-0.3,10.,5.57606079858305));
#8285=CARTESIAN_POINT('',(-0.3,12.8,5.88));
#8286=CARTESIAN_POINT('',(-0.3,12.8,5.88));
#8287=CARTESIAN_POINT('',(-0.3,10.8,5.88));
#8288=CARTESIAN_POINT('',(-0.3,10.8,5.88));
#8289=CARTESIAN_POINT('',(-0.3,10.8,5.88));
#8290=CARTESIAN_POINT('Origin',(0.,10.8,5.655));
#8291=CARTESIAN_POINT('',(0.3,10.8,5.57606079858305));
#8292=CARTESIAN_POINT('Origin',(0.,10.8,6.53));
#8293=CARTESIAN_POINT('',(0.3,10.8,5.88));
#8294=CARTESIAN_POINT('',(0.3,10.8,5.88));
#8295=CARTESIAN_POINT('',(0.3,10.8,5.43));
#8296=CARTESIAN_POINT('Origin',(0.3,10.8,5.88));
#8297=CARTESIAN_POINT('',(0.3,12.8,5.57606079858305));
#8298=CARTESIAN_POINT('',(0.3,10.,5.57606079858305));
#8299=CARTESIAN_POINT('',(0.3,12.8,5.88));
#8300=CARTESIAN_POINT('',(0.3,10.8,5.88));
#8301=CARTESIAN_POINT('',(0.3,12.8,5.43));
#8302=CARTESIAN_POINT('Origin',(-0.3,10.8,5.88));
#8303=CARTESIAN_POINT('',(0.3,12.8,5.88));
#8304=CARTESIAN_POINT('Origin',(0.,12.8,5.655));
#8305=CARTESIAN_POINT('Origin',(0.,12.8,6.53));
#8306=CARTESIAN_POINT('Origin',(0.,10.,6.53));
#8307=CARTESIAN_POINT('',(-1.,24.5,6.53));
#8308=CARTESIAN_POINT('Origin',(0.,24.5,6.53));
#8309=CARTESIAN_POINT('',(-1.,10.,6.53));
#8310=CARTESIAN_POINT('',(-1.,10.,6.53));
#8311=CARTESIAN_POINT('Origin',(0.,10.,6.53));
#8312=CARTESIAN_POINT('Origin',(0.,24.5,6.53));
#8313=CARTESIAN_POINT('Origin',(0.,10.,6.53));
#9096=UNCERTAINTY_MEASURE_WITH_UNIT(LENGTH_MEASURE(0.001),#9142,
'DISTANCE_ACCURACY_VALUE',
'Maximum model space distance between geometric entities at asserted c
onnectivities');
#9108=UNCERTAINTY_MEASURE_WITH_UNIT(LENGTH_MEASURE(0.001),#9142,
'DISTANCE_ACCURACY_VALUE',
'Maximum model space distance between geometric entities at asserted c
onnectivities');
#9129=(
GEOMETRIC_REPRESENTATION_CONTEXT(3)
GLOBAL_UNCERTAINTY_ASSIGNED_CONTEXT((#9096))
GLOBAL_UNIT_ASSIGNED_CONTEXT((#9142,#9144,#9145))
REPRESENTATION_CONTEXT('','3D')
);
#9141=(
GEOMETRIC_REPRESENTATION_CONTEXT(3)
GLOBAL_UNCERTAINTY_ASSIGNED_CONTEXT((#9108))
GLOBAL_UNIT_ASSIGNED_CONTEXT((#9142,#9144,#9145))
REPRESENTATION_CONTEXT('','3D')
);
#9142=(
LENGTH_UNIT()
NAMED_UNIT(*)
SI_UNIT(.CENTI.,.METRE.)
);
#9144=(
NAMED_UNIT(*)
PLANE_ANGLE_UNIT()
SI_UNIT($,.RADIAN.)
);
#9145=(
NAMED_UNIT(*)
SI_UNIT($,.STERADIAN.)
SOLID_ANGLE_UNIT()
);
#9166=SHAPE_DEFINITION_REPRESENTATION(#9200,#9294);
#9200=PRODUCT_DEFINITION_SHAPE('',$,#9327);
#9294=SHAPE_REPRESENTATION('',(#5372),#9129);
#9306=PRODUCT_DEFINITION_CONTEXT('part definition',#9404,'design');
#9327=PRODUCT_DEFINITION('Shaft stub (1)','Shaft stub (1)',#9359,#9306);
#9359=PRODUCT_DEFINITION_FORMATION('',$,#9426);
#9404=APPLICATION_CONTEXT(
'Core Data for Automotive Mechanical Design Process');
#9405=PRODUCT_CONTEXT('part definition',#9404,'mechanical');
#9426=PRODUCT('Shaft stub (1)','Shaft stub (1)','Shaft stub (1)',(#9405));
#9494=COLOUR_RGB('Grey',0.48,0.52,0.57);
#9495=FILL_AREA_STYLE_COLOUR('',#9494);
#9496=FILL_AREA_STYLE('',(#9495));
#9497=SURFACE_STYLE_FILL_AREA(#9496);
#9498=SURFACE_SIDE_STYLE('',(#9497));
#9499=SURFACE_STYLE_USAGE(.BOTH.,#9498);
#9500=PRESENTATION_STYLE_ASSIGNMENT((#9499));
ENDSEC;
END-ISO-10303-21;
